ISO-10303-21;
HEADER;
/* Generated by software containing ST-Developer
 * from STEP Tools, Inc. (www.steptools.com) 
 */

FILE_DESCRIPTION(
/* description */ (''),
/* implementation_level */ '2;1');

FILE_NAME(
/* name */ '11_Cover_O-Ring_147x3.step',
/* time_stamp */ '2026-10-26T04:15:57-07:00',
/* author */ (''),
/* organization */ (''),
/* preprocessor_version */ 'ST-DEVELOPER v20.2',
/* originating_system */ 'Autodesk Translation Framework v15.15.0.0',
/* authorisation */ '');

FILE_SCHEMA (('AUTOMOTIVE_DESIGN { 1 0 10303 214 3 1 1 }'));
ENDSEC;

DATA;
#10=MECHANICAL_DESIGN_GEOMETRIC_PRESENTATION_REPRESENTATION('',(#462),#55737);
#422=SHAPE_REPRESENTATION_RELATIONSHIP('SRR','None',#55831,#442);
#442=ADVANCED_BREP_SHAPE_REPRESENTATION('',(#482),#55727);
#462=STYLED_ITEM('',(#55998),#482);
#482=MANIFOLD_SOLID_BREP('Body1',#27231);
#7855=FACE_OUTER_BOUND('',#9524,.T.);
#9524=EDGE_LOOP('',(#23002,#23003,#23004,#23005));
#10780=CIRCLE('',#29198,1.5);
#10781=CIRCLE('',#29199,72.);
#13091=VERTEX_POINT('',#45276);
#16505=EDGE_CURVE('',#13091,#13091,#10780,.T.);
#16506=EDGE_CURVE('',#13091,#13091,#10781,.T.);
#23002=ORIENTED_EDGE('',*,*,#16505,.F.);
#23003=ORIENTED_EDGE('',*,*,#16506,.T.);
#23004=ORIENTED_EDGE('',*,*,#16505,.T.);
#23005=ORIENTED_EDGE('',*,*,#16506,.F.);
#25650=TOROIDAL_SURFACE('',#29197,73.5,1.5);
#26679=ADVANCED_FACE('',(#7855),#25650,.T.);
#27231=CLOSED_SHELL('',(#26679));
#29196=AXIS2_PLACEMENT_3D('',#45274,#35026,#35027);
#29197=AXIS2_PLACEMENT_3D('',#45275,#35028,#35029);
#29198=AXIS2_PLACEMENT_3D('',#45277,#35030,#35031);
#29199=AXIS2_PLACEMENT_3D('',#45278,#35032,#35033);
#35026=DIRECTION('axis',(0.,0.,1.));
#35027=DIRECTION('refdir',(1.,0.,0.));
#35028=DIRECTION('center_axis',(1.,0.,0.));
#35029=DIRECTION('ref_axis',(0.,0.,-1.));
#35030=DIRECTION('center_axis',(0.,-1.,-1.22464679914735E-16));
#35031=DIRECTION('ref_axis',(0.,-1.22464679914735E-16,1.));
#35032=DIRECTION('center_axis',(-1.,0.,0.));
#35033=DIRECTION('ref_axis',(0.,0.,-1.));
#45274=CARTESIAN_POINT('',(0.,0.,0.));
#45275=CARTESIAN_POINT('Origin',(-1.5,0.,0.));
#45276=CARTESIAN_POINT('',(-1.5,-8.81745695386094E-15,72.));
#45277=CARTESIAN_POINT('Origin',(-1.5,-9.00115397373305E-15,73.5));
#45278=CARTESIAN_POINT('Origin',(-1.5,0.,0.));
#55705=UNCERTAINTY_MEASURE_WITH_UNIT(LENGTH_MEASURE(0.01),#55738,
'DISTANCE_ACCURACY_VALUE',
'Maximum model space distance between geometric entities at asserted c
onnectivities');
#55715=UNCERTAINTY_MEASURE_WITH_UNIT(LENGTH_MEASURE(0.01),#55738,
'DISTANCE_ACCURACY_VALUE',
'Maximum model space distance between geometric entities at asserted c
onnectivities');
#55727=(
GEOMETRIC_REPRESENTATION_CONTEXT(3)
GLOBAL_UNCERTAINTY_ASSIGNED_CONTEXT((#55705))
GLOBAL_UNIT_ASSIGNED_CONTEXT((#55738,#55740,#55741))
REPRESENTATION_CONTEXT('','3D')
);
#55737=(
GEOMETRIC_REPRESENTATION_CONTEXT(3)
GLOBAL_UNCERTAINTY_ASSIGNED_CONTEXT((#55715))
GLOBAL_UNIT_ASSIGNED_CONTEXT((#55738,#55740,#55741))
REPRESENTATION_CONTEXT('','3D')
);
#55738=(
LENGTH_UNIT()
NAMED_UNIT(*)
SI_UNIT(.MILLI.,.METRE.)
);
#55740=(
NAMED_UNIT(*)
PLANE_ANGLE_UNIT()
SI_UNIT($,.RADIAN.)
);
#55741=(
NAMED_UNIT(*)
SI_UNIT($,.STERADIAN.)
SOLID_ANGLE_UNIT()
);
#55753=SHAPE_DEFINITION_REPRESENTATION(#55774,#55831);
#55774=PRODUCT_DEFINITION_SHAPE('',$,#55853);
#55831=SHAPE_REPRESENTATION('',(#29196),#55727);
#55841=PRODUCT_DEFINITION_CONTEXT('part definition',#55906,'design');
#55853=PRODUCT_DEFINITION('2026-10-26-00-34-26-328',
'11_Cover_O-Ring_147x3',#55874,#55841);
#55874=PRODUCT_DEFINITION_FORMATION('',$,#55919);
#55906=APPLICATION_CONTEXT(
'Core Data for Automotive Mechanical Design Process');
#55907=PRODUCT_CONTEXT('part definition',#55906,'mechanical');
#55919=PRODUCT('2026-10-26-00-34-26-328','11_Cover_O-Ring_147x3',$,(#55907));
#55992=COLOUR_RGB('Black',0.12,0.14,0.17);
#55993=FILL_AREA_STYLE_COLOUR('',#55992);
#55994=FILL_AREA_STYLE('',(#55993));
#55995=SURFACE_STYLE_FILL_AREA(#55994);
#55996=SURFACE_SIDE_STYLE('',(#55995));
#55997=SURFACE_STYLE_USAGE(.BOTH.,#55996);
#55998=PRESENTATION_STYLE_ASSIGNMENT((#55997));
ENDSEC;
END-ISO-10303-21;
